ISO-10303-21;
HEADER;
FILE_DESCRIPTION (('STEP AP214'),
    '1' );
FILE_NAME ('Rotary Valve Ball.step',
    '2026-10-09T13:48:35',
    ( '' ),
    ( '' ),
    'SwSTEP 2.0',
    'SolidWorks 2026',
    '' );
FILE_SCHEMA (( 'AUTOMOTIVE_DESIGN' ));
ENDSEC;

DATA;
#32=DIRECTION ( 'NONE',  ( 0.000000000000000000, 0.000000000000000000, -1.000000000000000000 ) ) ;
#180=EDGE_CURVE ( 'NONE', #2621, #20551, #276, .T. ) ;
#206=CARTESIAN_POINT ( 'NONE',  ( 1.709999999999999964, 9.000000000000000000, -7.500000000000000000 ) ) ;
#228=CIRCLE ( 'NONE', #16200, 9.999999999999996447 ) ;
#241=FACE_OUTER_BOUND ( 'NONE', #11847, .T. ) ;
#257=CARTESIAN_POINT ( 'NONE',  ( 1.660953982101407433, 6.978325578095221360, -0.5614028787491848194 ) ) ;
#276=CIRCLE ( 'NONE', #20030, 12.34057940292999511 ) ;
#282=AXIS2_PLACEMENT_3D ( 'NONE', #22952, #17521, #14002 ) ;
#380=ORIENTED_EDGE ( 'NONE', *, *, #4764, .F. ) ;
#454=CIRCLE ( 'NONE', #17487, 7.000000000000000000 ) ;
#459=CARTESIAN_POINT ( 'NONE',  ( -1.433806482797786552, 6.927073644917858708, 1.013309697580697222 ) ) ;
#469=ORIENTED_EDGE ( 'NONE', *, *, #7744, .F. ) ;
#497=CARTESIAN_POINT ( 'NONE',  ( 0.4206857880311101749, 6.789717089907916225, -1.702993728068331825 ) ) ;
#511=EDGE_CURVE ( 'NONE', #20864, #19479, #19182, .T. ) ;
#575=CARTESIAN_POINT ( 'NONE',  ( -0.3507184568084537046, 6.786897298932621503, 1.714069254809378551 ) ) ;
#627=EDGE_CURVE ( 'NONE', #19479, #13618, #15418, .T. ) ;
#699=ORIENTED_EDGE ( 'NONE', *, *, #1410, .F. ) ;
#703=CARTESIAN_POINT ( 'NONE',  ( 0.1193520287149335557, 6.778461007907296221, 1.747140996228561338 ) ) ;
#763=EDGE_CURVE ( 'NONE', #9475, #2621, #228, .T. ) ;
#826=CARTESIAN_POINT ( 'NONE',  ( 0.3327206652627045513, 6.785866010577869645, 1.718147026174522196 ) ) ;
#912=EDGE_CURVE ( 'NONE', #2993, #13096, #18112, .T. ) ;
#947=CARTESIAN_POINT ( 'NONE',  ( 0.2465075831868113188, 6.782055991726995359, 1.733133522506556057 ) ) ;
#959=VERTEX_POINT ( 'NONE', #12646 ) ;
#1011=CIRCLE ( 'NONE', #16100, 7.000000000000000000 ) ;
#1038=ORIENTED_EDGE ( 'NONE', *, *, #627, .T. ) ;
#1086=PLANE ( 'NONE',  #5614 ) ;
#1106=DIRECTION ( 'NONE',  ( 0.000000000000000000, 1.000000000000000000, 0.000000000000000000 ) ) ;
#1134=B_SPLINE_CURVE_WITH_KNOTS ( 'NONE', 3,
 ( #4597, #6278, #11858, #13423, #13661, #13910, #19241, #2654, #459, #20823, #2525, #17549, #9796, #22982, #8112, #4720, #17179, #19371, #19494, #20943, #10047, #21307, #10283, #575, #17432, #7982, #17303, #703, #15595, #947, #8343, #15354, #826, #6525, #6160, #8226, #4348, #6398, #11739, #13781, #15837, #14506, #5086, #21785, #8590, #3151, #20094, #10532, #19741, #8839 ),
 .UNSPECIFIED., .F., .F.,
 ( 4, 2, 2, 2, 2, 2, 2, 2, 2, 2, 1, 2, 2, 2, 2, 1, 2, 2, 2, 2, 2, 2, 2, 2, 2, 4 ),
 ( 0.000000000000000000, 0.06250000000000036082, 0.09375000000000056899, 0.1250000000000007772, 0.1875000000000012490, 0.2187500000000014155, 0.2343750000000014155, 0.2500000000000014433, 0.3125000000000014433, 0.3437500000000014433, 0.3593750000000013878, 0.3671875000000013878, 0.3750000000000013878, 0.4375000000000011657, 0.4687500000000011102, 0.4843750000000009992, 0.4921875000000009992, 0.5000000000000009992, 0.5625000000000007772, 0.6250000000000005551, 0.6875000000000005551, 0.7500000000000004441, 0.8125000000000003331, 0.8437500000000003331, 0.8750000000000002220, 1.000000000000000000 ),
 .UNSPECIFIED. ) ;
#1200=ADVANCED_FACE ( 'NONE', ( #15753 ), #8625, .F. ) ;
#1296=EDGE_LOOP ( 'NONE', ( #5419, #8368, #9608, #1038, #2352, #17879, #3376 ) ) ;
#1329=VERTEX_POINT ( 'NONE', #17591 ) ;
#1410=EDGE_CURVE ( 'NONE', #7085, #18414, #4413, .T. ) ;
#1505=COLOUR_RGB ( '', 0.08235294, 0.09019608, 0.10196078) ;
#1534=ORIENTED_EDGE ( 'NONE', *, *, #2121, .F. ) ;
#1536=EDGE_LOOP ( 'NONE', ( #8202, #9301 ) ) ;
#1568=EDGE_CURVE ( 'NONE', #20019, #13096, #454, .T. ) ;
#1569=EDGE_CURVE ( 'NONE', #12723, #13227, #7816, .T. ) ;
#1580=FACE_OUTER_BOUND ( 'NONE', #8119, .T. ) ;
#1604=ORIENTED_EDGE ( 'NONE', *, *, #180, .T. ) ;
#1638=AXIS2_PLACEMENT_3D ( 'NONE', #20243, #3647, #20477 ) ;
#1683=AXIS2_PLACEMENT_3D ( 'NONE', #15512, #19281, #10081 ) ;
#1690=CARTESIAN_POINT ( 'NONE',  ( 7.500000000000000000, -10.00000000000000000, 0.000000000000000000 ) ) ;
#1749=AXIS2_PLACEMENT_3D ( 'NONE', #21319, #2915, #23114 ) ;
#1806=AXIS2_PLACEMENT_3D ( 'NONE', #5878, #20902, #13149 ) ;
#1821=CARTESIAN_POINT ( 'NONE',  ( 0.000000000000000000, 0.000000000000000000, 0.000000000000000000 ) ) ;
#1974=CARTESIAN_POINT ( 'NONE',  ( 1.524598462963647538, 6.946544218151612604, -0.8912506324979003747 ) ) ;
#2072=DIRECTION ( 'NONE',  ( 0.000000000000000000, 1.000000000000000000, 0.000000000000000000 ) ) ;
#2076=VERTEX_POINT ( 'NONE', #2150 ) ;
#2111=ORIENTED_EDGE ( 'NONE', *, *, #19314, .T. ) ;
#2121=EDGE_CURVE ( 'NONE', #1329, #12723, #11841, .T. ) ;
#2150=CARTESIAN_POINT ( 'NONE',  ( 1.709999999999999964, 9.000000000000000000, 7.500000000000000000 ) ) ;
#2300=SURFACE_STYLE_FILL_AREA ( #2533 ) ;
#2314=ORIENTED_EDGE ( 'NONE', *, *, #6712, .T. ) ;
#2327=CARTESIAN_POINT ( 'NONE',  ( 0.7010477225544974322, 6.813607535519789593, -1.604763118501952412 ) ) ;
#2351=CARTESIAN_POINT ( 'NONE',  ( 1.709999999999999964, 9.000000000000000000, -7.500000000000000000 ) ) ;
#2352=ORIENTED_EDGE ( 'NONE', *, *, #23275, .T. ) ;
#2390=AXIS2_PLACEMENT_3D ( 'NONE', #12324, #19715, #23689 ) ;
#2412=ORIENTED_EDGE ( 'NONE', *, *, #20628, .F. ) ;
#2440=ORIENTED_EDGE ( 'NONE', *, *, #9146, .T. ) ;
#2460=CARTESIAN_POINT ( 'NONE',  ( 1.709999999999999964, 9.852710287022999225, -7.500000000000000000 ) ) ;
#2471=DIRECTION ( 'NONE',  ( -1.000000000000000000, 0.000000000000000000, 0.000000000000000000 ) ) ;
#2490=FACE_OUTER_BOUND ( 'NONE', #18572, .T. ) ;
#2518=ORIENTED_EDGE ( 'NONE', *, *, #4350, .F. ) ;
#2520=FACE_OUTER_BOUND ( 'NONE', #11992, .T. ) ;
#2525=CARTESIAN_POINT ( 'NONE',  ( -1.257898175673276331, 6.893178841067931550, 1.219165795350648285 ) ) ;
#2533=FILL_AREA_STYLE ('',( #22630 ) ) ;
#2580=CIRCLE ( 'NONE', #18829, 1.750000000000000444 ) ;
#2621=VERTEX_POINT ( 'NONE', #18564 ) ;
#2648=CARTESIAN_POINT ( 'NONE',  ( 0.000000000000000000, -13.00000000000000000, 0.000000000000000000 ) ) ;
#2654=CARTESIAN_POINT ( 'NONE',  ( -1.507771686977886771, 6.943202342706179309, 0.8987492179439539042 ) ) ;
#2664=CIRCLE ( 'NONE', #5003, 12.34057940292999866 ) ;
#2674=AXIS2_PLACEMENT_3D ( 'NONE', #5106, #21695, #3048 ) ;
#2698=ORIENTED_EDGE ( 'NONE', *, *, #180, .F. ) ;
#2703=AXIS2_PLACEMENT_3D ( 'NONE', #11095, #9280, #10977 ) ;
#2772=DIRECTION ( 'NONE',  ( 0.000000000000000000, 1.000000000000000000, 0.000000000000000000 ) ) ;
#2774=ORIENTED_EDGE ( 'NONE', *, *, #1568, .F. ) ;
#2775=FACE_OUTER_BOUND ( 'NONE', #11419, .T. ) ;
#2811=CIRCLE ( 'NONE', #7827, 12.50000000000000000 ) ;
#2820=ADVANCED_FACE ( 'NONE', ( #17585 ), #9827, .F. ) ;
#2915=DIRECTION ( 'NONE',  ( 1.000000000000000000, 0.000000000000000000, 0.000000000000000000 ) ) ;
#2944=AXIS2_PLACEMENT_3D ( 'NONE', #3071, #17720, #8519 ) ;
#2953=DIRECTION ( 'NONE',  ( 0.000000000000000000, 1.000000000000000000, 0.000000000000000000 ) ) ;
#2977=ORIENTED_EDGE ( 'NONE', *, *, #5483, .T. ) ;
#2993=VERTEX_POINT ( 'NONE', #7382 ) ;
#3020=CARTESIAN_POINT ( 'NONE',  ( -12.75000000000000000, 0.000000000000000000, 0.000000000000000000 ) ) ;
#3048=DIRECTION ( 'NONE',  ( 0.000000000000000000, -1.000000000000000000, 0.000000000000000000 ) ) ;
#3050=DIRECTION ( 'NONE',  ( 1.000000000000000000, 0.000000000000000000, 0.000000000000000000 ) ) ;
#3071=CARTESIAN_POINT ( 'NONE',  ( -10.35615758860000035, 0.000000000000000000, 0.000000000000000000 ) ) ;
#3151=CARTESIAN_POINT ( 'NONE',  ( 1.612461263175861692, 6.966911249336811274, 0.6814213867173207761 ) ) ;
#3201=CARTESIAN_POINT ( 'NONE',  ( -1.750000000000000000, 7.000000000000000000, 0.000000000000000000 ) ) ;
#3237=ORIENTED_EDGE ( 'NONE', *, *, #23888, .F. ) ;
#3254=CARTESIAN_POINT ( 'NONE',  ( 0.000000000000000000, -9.000000000000000000, 0.000000000000000000 ) ) ;
#3293=EDGE_CURVE ( 'NONE', #959, #15568, #1134, .T. ) ;
#3320=CIRCLE ( 'NONE', #21858, 1.750000000000000000 ) ;
#3363=VECTOR ( 'NONE', #2471, 1000.000000000000000 ) ;
#3376=ORIENTED_EDGE ( 'NONE', *, *, #21054, .T. ) ;
#3388=CIRCLE ( 'NONE', #9163, 12.50000000000000000 ) ;
#3412=ORIENTED_EDGE ( 'NONE', *, *, #15473, .T. ) ;
#3446=CARTESIAN_POINT ( 'NONE',  ( 0.000000000000000000, -10.00000000000000000, 0.000000000000000000 ) ) ;
#3479=EDGE_CURVE ( 'NONE', #20864, #20904, #2580, .T. ) ;
#3532=CARTESIAN_POINT ( 'NONE',  ( 1.709999999999999964, 12.37689379448999993, 0.3720215047547999476 ) ) ;
#3647=DIRECTION ( 'NONE',  ( -1.000000000000000000, 0.000000000000000000, 0.000000000000000000 ) ) ;
#3673=CARTESIAN_POINT ( 'NONE',  ( -0.4421657205835797244, 6.791814712419944833, -1.694527932936234604 ) ) ;
#3674=DIRECTION ( 'NONE',  ( 0.1400000000000034828, 0.9901515035589245617, 0.000000000000000000 ) ) ;
#3713=LINE ( 'NONE', #19841, #10401 ) ;
#3758=DIRECTION ( 'NONE',  ( 1.000000000000000000, 0.000000000000000000, 0.000000000000000000 ) ) ;
#3873=EDGE_LOOP ( 'NONE', ( #3237, #4591, #23086, #17175 ) ) ;
#3902=CARTESIAN_POINT ( 'NONE',  ( 1.709999999999999964, 9.000000000000000000, -0.3720215047547999476 ) ) ;
#3999=SURFACE_STYLE_USAGE ( .BOTH. , #18765 ) ;
#4013=ORIENTED_EDGE ( 'NONE', *, *, #22806, .F. ) ;
#4143=CARTESIAN_POINT ( 'NONE',  ( 1.750000000000001998, 7.000000000000000888, -0.1151749530721415948 ) ) ;
#4169=VECTOR ( 'NONE', #21020, 1000.000000000000000 ) ;
#4171=DIRECTION ( 'NONE',  ( 0.000000000000000000, 0.000000000000000000, -1.000000000000000000 ) ) ;
#4292=ORIENTED_EDGE ( 'NONE', *, *, #912, .F. ) ;
#4306=CARTESIAN_POINT ( 'NONE',  ( 1.750000000000000000, 7.000000000000000000, 0.000000000000000000 ) ) ;
#4342=DIRECTION ( 'NONE',  ( 0.000000000000000000, 1.000000000000000000, 0.000000000000000000 ) ) ;
#4348=CARTESIAN_POINT ( 'NONE',  ( 0.8157680887313131235, 6.826070574582712602, 1.551609257856797930 ) ) ;
#4350=EDGE_CURVE ( 'NONE', #2621, #20340, #14969, .T. ) ;
#4390=AXIS2_PLACEMENT_3D ( 'NONE', #8983, #23856, #3758 ) ;
#4403=ORIENTED_EDGE ( 'NONE', *, *, #627, .F. ) ;
#4413=CIRCLE ( 'NONE', #17968, 12.38248359579000279 ) ;
#4432=DIRECTION ( 'NONE',  ( 0.000000000000000000, 0.000000000000000000, -1.000000000000000000 ) ) ;
#4464=CYLINDRICAL_SURFACE ( 'NONE', #7296, 1.750000000000000000 ) ;
#4478=( LENGTH_UNIT ( ) NAMED_UNIT ( * ) SI_UNIT ( .MILLI., .METRE. ) );
#4509=EDGE_CURVE ( 'NONE', #5868, #7294, #13430, .T. ) ;
#4534=SPHERICAL_SURFACE ( 'NONE', #9177, 12.50000000000000000 ) ;
#4539=CARTESIAN_POINT ( 'NONE',  ( -7.500000000000000000, -10.00000000000000000, 0.000000000000000000 ) ) ;
#4591=ORIENTED_EDGE ( 'NONE', *, *, #21054, .F. ) ;
#4596=AXIS2_PLACEMENT_3D ( 'NONE', #3446, #21842, #5255 ) ;
#4597=CARTESIAN_POINT ( 'NONE',  ( -1.750000000000000000, 7.000000000000000000, 0.000000000000000000 ) ) ;
#4635=CARTESIAN_POINT ( 'NONE',  ( -1.419111322447411450, 6.922937340745385804, -1.049103944711770708 ) ) ;
#4670=CARTESIAN_POINT ( 'NONE',  ( 1.709999999999999964, 9.852710287022999225, 7.500000000000000000 ) ) ;
#4720=CARTESIAN_POINT ( 'NONE',  ( -0.9439381825837785955, 6.842295547824369883, 1.479774886885111274 ) ) ;
#4727=ORIENTED_EDGE ( 'NONE', *, *, #3293, .T. ) ;
#4764=EDGE_CURVE ( 'NONE', #20551, #5868, #20195, .T. ) ;
#4783=AXIS2_PLACEMENT_3D ( 'NONE', #12261, #12387, #17949 ) ;
#4828=LINE ( 'NONE', #8215, #16948 ) ;
#4835=CIRCLE ( 'NONE', #7915, 7.500000000000000000 ) ;
#4897=CARTESIAN_POINT ( 'NONE',  ( 1.709999999999999964, 9.000000000000000000, -0.3720215047547999476 ) ) ;
#4925=CARTESIAN_POINT ( 'NONE',  ( -1.989999999999999991, 9.000000000000000000, 7.500000000000000000 ) ) ;
#4979=DIRECTION ( 'NONE',  ( 1.000000000000000000, 0.000000000000000000, 0.000000000000000000 ) ) ;
#5003=AXIS2_PLACEMENT_3D ( 'NONE', #19478, #17659, #6870 ) ;
#5038=PLANE ( 'NONE',  #10131 ) ;
#5076=PLANE ( 'NONE',  #23166 ) ;
#5086=CARTESIAN_POINT ( 'NONE',  ( 1.472041947694723518, 6.935496243266504379, 0.9522668941083732852 ) ) ;
#5098=CYLINDRICAL_SURFACE ( 'NONE', #1749, 7.000000000000000000 ) ;
#5106=CARTESIAN_POINT ( 'NONE',  ( -10.35615758860000035, 0.000000000000000000, 0.000000000000000000 ) ) ;
#5113=ADVANCED_FACE ( 'NONE', ( #21620 ), #5038, .T. ) ;
#5115=CARTESIAN_POINT ( 'NONE',  ( -10.35615758860000035, 0.000000000000000000, 0.000000000000000000 ) ) ;
#5255=DIRECTION ( 'NONE',  ( -1.000000000000000000, 0.000000000000000000, 0.000000000000000000 ) ) ;
#5341=AXIS2_PLACEMENT_3D ( 'NONE', #22473, #4432, #22591 ) ;
#5376=AXIS2_PLACEMENT_3D ( 'NONE', #2648, #2772, #9172 ) ;
#5419=ORIENTED_EDGE ( 'NONE', *, *, #19027, .F. ) ;
#5465=DIRECTION ( 'NONE',  ( -1.000000000000000000, 0.000000000000000000, 0.000000000000000000 ) ) ;
#5483=EDGE_CURVE ( 'NONE', #9495, #21993, #15706, .T. ) ;
#5487=ORIENTED_EDGE ( 'NONE', *, *, #15103, .F. ) ;
#5513=ORIENTED_EDGE ( 'NONE', *, *, #23275, .F. ) ;
#5583=CARTESIAN_POINT ( 'NONE',  ( 0.000000000000000000, 9.000000000000000000, 0.000000000000000000 ) ) ;
#5614=AXIS2_PLACEMENT_3D ( 'NONE', #12120, #8486, #23488 ) ;
#5670=ORIENTED_EDGE ( 'NONE', *, *, #18187, .F. ) ;
#5685=CARTESIAN_POINT ( 'NONE',  ( -7.500000000000000000, -9.000000000000000000, 0.000000000000000000 ) ) ;
#5710=CIRCLE ( 'NONE', #6493, 7.500000000000000000 ) ;
#5868=VERTEX_POINT ( 'NONE', #20421 ) ;
#5878=CARTESIAN_POINT ( 'NONE',  ( 0.000000000000000000, 0.000000000000000000, 0.000000000000000000 ) ) ;
#5991=CARTESIAN_POINT ( 'NONE',  ( 1.709999999999999964, 0.000000000000000000, 0.000000000000000000 ) ) ;
#6068=CARTESIAN_POINT ( 'NONE',  ( -0.6904636124130929531, 6.812739684286071018, -1.608326952461486714 ) ) ;
#6160=CARTESIAN_POINT ( 'NONE',  ( 0.5400519283707410079, 6.798561526091877916, 1.667608383989048759 ) ) ;
#6185=LINE ( 'NONE', #12013, #23825 ) ;
#6196=CARTESIAN_POINT ( 'NONE',  ( -0.9206838382964129819, 6.836823221689457775, -1.505541136744114938 ) ) ;
#6221=CARTESIAN_POINT ( 'NONE',  ( 0.000000000000000000, 0.000000000000000000, 0.000000000000000000 ) ) ;
#6278=CARTESIAN_POINT ( 'NONE',  ( -1.750000000000000222, 7.000000000000004441, 0.1353757534095987036 ) ) ;
#6302=ORIENTED_EDGE ( 'NONE', *, *, #7433, .T. ) ;
#6387=VECTOR ( 'NONE', #4979, 1000.000000000000000 ) ;
#6398=CARTESIAN_POINT ( 'NONE',  ( 0.9858775068236067529, 6.848474835707053288, 1.449525164644654751 ) ) ;
#6409=DIRECTION ( 'NONE',  ( 0.000000000000000000, -1.000000000000000000, 0.000000000000000000 ) ) ;
#6436=CARTESIAN_POINT ( 'NONE',  ( -1.750000000000000000, 7.000000000000000000, -0.2229454749283412696 ) ) ;
#6482=APPLICATION_CONTEXT ( 'automotive_design' ) ;
#6493=AXIS2_PLACEMENT_3D ( 'NONE', #16290, #8564, #17890 ) ;
#6525=CARTESIAN_POINT ( 'NONE',  ( 0.4441971634758341003, 6.791582890693172558, 1.695532875298955355 ) ) ;
#6563=CARTESIAN_POINT ( 'NONE',  ( -0.6075102312704570018, 6.804820720190284611, -1.641503610285228065 ) ) ;
#6597=PLANE ( 'NONE',  #13745 ) ;
#6616=PLANE ( 'NONE',  #282 ) ;
#6647=ORIENTED_EDGE ( 'NONE', *, *, #912, .T. ) ;
#6712=EDGE_CURVE ( 'NONE', #20551, #12102, #2664, .T. ) ;
#6759=DIRECTION ( 'NONE',  ( 1.000000000000000000, 0.000000000000000000, 0.000000000000000000 ) ) ;
#6818=EDGE_LOOP ( 'NONE', ( #18981, #5487, #2518, #10269 ) ) ;
#6870=DIRECTION ( 'NONE',  ( 0.000000000000000000, 1.000000000000000000, 0.000000000000000000 ) ) ;
#7019=LINE ( 'NONE', #18051, #6387 ) ;
#7085=VERTEX_POINT ( 'NONE', #22811 ) ;
#7152=ADVANCED_FACE ( 'NONE', ( #16021 ), #6597, .F. ) ;
#7230=VECTOR ( 'NONE', #2953, 1000.000000000000000 ) ;
#7232=ORIENTED_EDGE ( 'NONE', *, *, #17985, .F. ) ;
#7294=VERTEX_POINT ( 'NONE', #13116 ) ;
#7296=AXIS2_PLACEMENT_3D ( 'NONE', #23096, #4342, #13655 ) ;
#7322=ORIENTED_EDGE ( 'NONE', *, *, #6712, .F. ) ;
#7382=CARTESIAN_POINT ( 'NONE',  ( 1.750000000000000000, 12.37689379448999993, 0.000000000000000000 ) ) ;
#7414=DIRECTION ( 'NONE',  ( -0.8284926070883130711, -0.5600000000000090461, 0.000000000000000000 ) ) ;
#7433=EDGE_CURVE ( 'NONE', #12102, #7085, #16838, .T. ) ;
#7474=EDGE_CURVE ( 'NONE', #7294, #13433, #17638, .T. ) ;
#7621=DIRECTION ( 'NONE',  ( 0.8284926070883130711, -0.5600000000000090461, 0.000000000000000000 ) ) ;
#7643=CARTESIAN_POINT ( 'NONE',  ( 1.709999999999999964, 13.00000000000000000, -7.500000000000000000 ) ) ;
#7662=CARTESIAN_POINT ( 'NONE',  ( 0.5338398250025285785, 6.797827069970633573, -1.670807105909973167 ) ) ;
#7744=EDGE_CURVE ( 'NONE', #13227, #20019, #1011, .T. ) ;
#7781=CARTESIAN_POINT ( 'NONE',  ( 1.693959225995342432, 6.986248014536463380, -0.4526555866337934608 ) ) ;
#7795=DIRECTION ( 'NONE',  ( 0.000000000000000000, 1.000000000000000000, 0.000000000000000000 ) ) ;
#7816=CIRCLE ( 'NONE', #1638, 7.000000000000000000 ) ;
#7827=AXIS2_PLACEMENT_3D ( 'NONE', #9718, #14913, #7414 ) ;
#7899=CARTESIAN_POINT ( 'NONE',  ( 0.1910135035480641785, 6.779320233362403414, -1.743921721967714777 ) ) ;
#7915=AXIS2_PLACEMENT_3D ( 'NONE', #12490, #18060, #3050 ) ;
#7982=CARTESIAN_POINT ( 'NONE',  ( -0.1076860494153716596, 6.777623460670147537, 1.750377179531549254 ) ) ;
#8105=FACE_OUTER_BOUND ( 'NONE', #19148, .T. ) ;
#8112=CARTESIAN_POINT ( 'NONE',  ( -1.077644597311803620, 6.862813149403997670, 1.379208851604670993 ) ) ;
#8119=EDGE_LOOP ( 'NONE', ( #23908, #5513, #21313, #7322, #2698 ) ) ;
#8199=( NAMED_UNIT ( * ) SI_UNIT ( $, .STERADIAN. ) SOLID_ANGLE_UNIT ( ) );
#8202=ORIENTED_EDGE ( 'NONE', *, *, #14605, .F. ) ;
#8215=CARTESIAN_POINT ( 'NONE',  ( -1.989999999999999991, 9.799994897958001161, -7.500000000000000000 ) ) ;
#8221=CARTESIAN_POINT ( 'NONE',  ( 10.35615758860000035, -7.000000000000000000, 0.000000000000000000 ) ) ;
#8226=CARTESIAN_POINT ( 'NONE',  ( 0.7252905466825813052, 6.815733255002632163, 1.595975169937962956 ) ) ;
#8321=CARTESIAN_POINT ( 'NONE',  ( -10.35615758860000035, 0.000000000000000000, 0.000000000000000000 ) ) ;
#8343=CARTESIAN_POINT ( 'NONE',  ( 0.2887885109354977331, 6.783830813142102123, 1.726165157609700129 ) ) ;
#8368=ORIENTED_EDGE ( 'NONE', *, *, #3479, .F. ) ;
#8386=CARTESIAN_POINT ( 'NONE',  ( 7.500000000000000000, -9.000000000000000000, 0.000000000000000000 ) ) ;
#8442=FACE_OUTER_BOUND ( 'NONE', #6818, .T. ) ;
#8482=CARTESIAN_POINT ( 'NONE',  ( 10.35615758860000035, 0.000000000000000000, 0.000000000000000000 ) ) ;
#8486=DIRECTION ( 'NONE',  ( -1.000000000000000000, 0.000000000000000000, 0.000000000000000000 ) ) ;
#8519=DIRECTION ( 'NONE',  ( 0.000000000000000000, 0.000000000000000000, 1.000000000000000000 ) ) ;
#8547=DIRECTION ( 'NONE',  ( 1.000000000000000000, 0.000000000000000000, 0.000000000000000000 ) ) ;
#8562=ORIENTED_EDGE ( 'NONE', *, *, #3479, .T. ) ;
#8564=DIRECTION ( 'NONE',  ( 0.000000000000000000, 1.000000000000000000, 0.000000000000000000 ) ) ;
#8590=CARTESIAN_POINT ( 'NONE',  ( 1.570131409422825142, 6.957183850560507921, 0.7744548611195164467 ) ) ;
#8625=CYLINDRICAL_SURFACE ( 'NONE', #1683, 7.500000000000000000 ) ;
#8728=PRODUCT_DEFINITION ( 'UNKNOWN', '', #19075, #12589 ) ;
#8836=DIRECTION ( 'NONE',  ( 0.000000000000000000, 0.000000000000000000, -1.000000000000000000 ) ) ;
#8839=CARTESIAN_POINT ( 'NONE',  ( 1.750000000000000000, 7.000000000000000000, 0.000000000000000000 ) ) ;
#8980=DIRECTION ( 'NONE',  ( 1.000000000000000000, 0.000000000000000000, 0.000000000000000000 ) ) ;
#8983=CARTESIAN_POINT ( 'NONE',  ( 0.000000000000000000, 0.000000000000000000, 0.000000000000000000 ) ) ;
#9146=EDGE_CURVE ( 'NONE', #22807, #21993, #11798, .T. ) ;
#9163=AXIS2_PLACEMENT_3D ( 'NONE', #1821, #13189, #7621 ) ;
#9172=DIRECTION ( 'NONE',  ( 1.000000000000000000, 0.000000000000000000, 0.000000000000000000 ) ) ;
#9177=AXIS2_PLACEMENT_3D ( 'NONE', #6221, #23171, #13975 ) ;
#9280=DIRECTION ( 'NONE',  ( 0.000000000000000000, 1.000000000000000000, 0.000000000000000000 ) ) ;
#9301=ORIENTED_EDGE ( 'NONE', *, *, #9146, .F. ) ;
#9358=CARTESIAN_POINT ( 'NONE',  ( 1.139388574200934423, 6.872381371660192251, -1.333228779845821776 ) ) ;
#9360=ORIENTED_EDGE ( 'NONE', *, *, #20628, .T. ) ;
#9372=VERTEX_POINT ( 'NONE', #1690 ) ;
#9425=VECTOR ( 'NONE', #4171, 1000.000000000000000 ) ;
#9475=VERTEX_POINT ( 'NONE', #4670 ) ;
#9495=VERTEX_POINT ( 'NONE', #4539 ) ;
#9593=EDGE_LOOP ( 'NONE', ( #9360, #23423, #18342, #699 ) ) ;
#9608=ORIENTED_EDGE ( 'NONE', *, *, #511, .T. ) ;
#9691=DIRECTION ( 'NONE',  ( -1.000000000000000000, 0.000000000000000000, 0.000000000000000000 ) ) ;
#9718=CARTESIAN_POINT ( 'NONE',  ( 0.000000000000000000, 0.000000000000000000, 0.000000000000000000 ) ) ;
#9735=DIRECTION ( 'NONE',  ( 0.000000000000000000, -1.000000000000000000, 0.000000000000000000 ) ) ;
#9762=CARTESIAN_POINT ( 'NONE',  ( 1.709999999999999964, 9.000000000000000000, 0.3720215047547999476 ) ) ;
#9770=DIRECTION ( 'NONE',  ( 1.000000000000000000, 0.000000000000000000, 0.000000000000000000 ) ) ;
#9796=CARTESIAN_POINT ( 'NONE',  ( -1.158286564292558829, 6.875900300209513816, 1.312442925060462562 ) ) ;
#9804=( NAMED_UNIT ( * ) PLANE_ANGLE_UNIT ( ) SI_UNIT ( $, .RADIAN. ) );
#9827=PLANE ( 'NONE',  #17960 ) ;
#9840=CARTESIAN_POINT ( 'NONE',  ( 0.000000000000000000, 0.000000000000000000, -7.500000000000000000 ) ) ;
#9881=AXIS2_PLACEMENT_3D ( 'NONE', #7643, #19388, #12125 ) ;
#9972=EDGE_CURVE ( 'NONE', #2993, #18414, #16235, .T. ) ;
#10047=CARTESIAN_POINT ( 'NONE',  ( -0.4498711834209865867, 6.792576835581316530, 1.691454280765045448 ) ) ;
#10081=DIRECTION ( 'NONE',  ( 1.000000000000000000, 0.000000000000000000, 0.000000000000000000 ) ) ;
#10098=EDGE_CURVE ( 'NONE', #13096, #12723, #20490, .T. ) ;
#10131=AXIS2_PLACEMENT_3D ( 'NONE', #17986, #16143, #19396 ) ;
#10200=ORIENTED_EDGE ( 'NONE', *, *, #13389, .F. ) ;
#10269=ORIENTED_EDGE ( 'NONE', *, *, #763, .F. ) ;
#10283=CARTESIAN_POINT ( 'NONE',  ( -0.3690988594039858461, 6.787862677517462195, 1.710243926673669979 ) ) ;
#10355=DIRECTION ( 'NONE',  ( 0.000000000000000000, 0.000000000000000000, 1.000000000000000000 ) ) ;
#10401=VECTOR ( 'NONE', #16308, 1000.000000000000000 ) ;
#10478=VERTEX_POINT ( 'NONE', #9762 ) ;
#10532=CARTESIAN_POINT ( 'NONE',  ( 1.716345169325534714, 6.991441436340903870, 0.3950169913663518217 ) ) ;
#10731=DIRECTION ( 'NONE',  ( 0.000000000000000000, -1.000000000000000000, 0.000000000000000000 ) ) ;
#10933=ORIENTED_EDGE ( 'NONE', *, *, #7433, .F. ) ;
#10959=CARTESIAN_POINT ( 'NONE',  ( 1.709999999999999964, 9.852710287022999225, 7.500000000000000000 ) ) ;
#10977=DIRECTION ( 'NONE',  ( 1.000000000000000000, 0.000000000000000000, 0.000000000000000000 ) ) ;
#11051=ORIENTED_EDGE ( 'NONE', *, *, #4509, .F. ) ;
#11095=CARTESIAN_POINT ( 'NONE',  ( 0.000000000000000000, 12.37689379448999993, 0.000000000000000000 ) ) ;
#11200=EDGE_CURVE ( 'NONE', #12102, #13618, #4828, .T. ) ;
#11206=CIRCLE ( 'NONE', #2674, 7.000000000000000000 ) ;
#11287=DIRECTION ( 'NONE',  ( 1.000000000000000000, 0.000000000000000000, 0.000000000000000000 ) ) ;
#11294=CARTESIAN_POINT ( 'NONE',  ( -1.750000000000000000, 9.000000000000000000, 0.000000000000000000 ) ) ;
#11304=CARTESIAN_POINT ( 'NONE',  ( 1.750000000000000000, 7.000000000000000000, 0.000000000000000000 ) ) ;
#11324=EDGE_CURVE ( 'NONE', #15568, #2993, #3713, .T. ) ;
#11362=ADVANCED_FACE ( 'NONE', ( #21663 ), #5076, .F. ) ;
#11411=DIRECTION ( 'NONE',  ( -1.000000000000000000, 0.000000000000000000, 0.000000000000000000 ) ) ;
#11419=EDGE_LOOP ( 'NONE', ( #2111, #469, #22619, #1534, #23017, #21440 ) ) ;
#11473=ORIENTED_EDGE ( 'NONE', *, *, #5483, .F. ) ;
#11504=DIRECTION ( 'NONE',  ( 0.000000000000000000, 1.000000000000000000, 0.000000000000000000 ) ) ;
#11540=CARTESIAN_POINT ( 'NONE',  ( 1.048658153906335100, 6.857636208004994849, -1.406037042848364838 ) ) ;
#11622=EDGE_CURVE ( 'NONE', #13433, #1329, #11206, .T. ) ;
#11659=CARTESIAN_POINT ( 'NONE',  ( -0.6619726575697483240, 6.809906748830050205, -1.620274423901518768 ) ) ;
#11681=ORIENTED_EDGE ( 'NONE', *, *, #1568, .T. ) ;
#11739=CARTESIAN_POINT ( 'NONE',  ( 1.065753921018558481, 6.860530577516010808, 1.391907256200018761 ) ) ;
#11762=ORIENTED_EDGE ( 'NONE', *, *, #10098, .F. ) ;
#11798=CIRCLE ( 'NONE', #16968, 7.500000000000000000 ) ;
#11841=LINE ( 'NONE', #23330, #12408 ) ;
#11847=EDGE_LOOP ( 'NONE', ( #12673, #4403, #2412, #10933 ) ) ;
#11858=CARTESIAN_POINT ( 'NONE',  ( -1.734941855790413712, 6.996073985788684446, 0.2676728999513400820 ) ) ;
#11866=( NAMED_UNIT ( * ) SI_UNIT ( $, .STERADIAN. ) SOLID_ANGLE_UNIT ( ) );
#11949=VECTOR ( 'NONE', #21244, 1000.000000000000000 ) ;
#11972=ORIENTED_EDGE ( 'NONE', *, *, #9972, .T. ) ;
#11992=EDGE_LOOP ( 'NONE', ( #22157, #2440, #11473, #5670 ) ) ;
#12013=CARTESIAN_POINT ( 'NONE',  ( 1.709999999999999964, 9.000000000000000000, 7.500000000000000000 ) ) ;
#12102=VERTEX_POINT ( 'NONE', #18237 ) ;
#12111=VECTOR ( 'NONE', #18886, 1000.000000000000000 ) ;
#12120=CARTESIAN_POINT ( 'NONE',  ( -1.989999999999999991, 13.00000000000000000, -7.500000000000000000 ) ) ;
#12125=DIRECTION ( 'NONE',  ( 0.000000000000000000, -1.000000000000000000, 0.000000000000000000 ) ) ;
#12174=CARTESIAN_POINT ( 'NONE',  ( 1.709999999999999964, 13.00000000000000000, 7.500000000000000000 ) ) ;
#12261=CARTESIAN_POINT ( 'NONE',  ( 0.000000000000000000, 12.37689379448999993, 0.000000000000000000 ) ) ;
#12323=ORIENTED_EDGE ( 'NONE', *, *, #22280, .F. ) ;
#12324=CARTESIAN_POINT ( 'NONE',  ( 0.000000000000000000, 0.000000000000000000, 0.000000000000000000 ) ) ;
#12387=DIRECTION ( 'NONE',  ( 0.000000000000000000, 1.000000000000000000, 0.000000000000000000 ) ) ;
#12408=VECTOR ( 'NONE', #17285, 1000.000000000000000 ) ;
#12490=CARTESIAN_POINT ( 'NONE',  ( 0.000000000000000000, -10.00000000000000000, 0.000000000000000000 ) ) ;
#12496=DIRECTION ( 'NONE',  ( 0.000000000000000000, 0.000000000000000000, -1.000000000000000000 ) ) ;
#12499=CARTESIAN_POINT ( 'NONE',  ( 1.709999999999999964, 9.000000000000000000, 0.3720215047547999476 ) ) ;
#12539=UNCERTAINTY_MEASURE_WITH_UNIT (LENGTH_MEASURE( 1.000000000000000082E-05 ), #21285, 'distance_accuracy_value', 'NONE');
#12577=ORIENTED_EDGE ( 'NONE', *, *, #23928, .F. ) ;
#12589=PRODUCT_DEFINITION_CONTEXT ( 'detailed design', #16691, 'design' ) ;
#12617=ORIENTED_EDGE ( 'NONE', *, *, #22792, .F. ) ;
#12646=CARTESIAN_POINT ( 'NONE',  ( -1.750000000000000000, 7.000000000000000000, 0.000000000000000000 ) ) ;
#12673=ORIENTED_EDGE ( 'NONE', *, *, #11200, .T. ) ;
#12679=AXIS2_PLACEMENT_3D ( 'NONE', #8321, #9770, #19215 ) ;
#12723=VERTEX_POINT ( 'NONE', #16456 ) ;
#12814=DIRECTION ( 'NONE',  ( 0.000000000000000000, 1.000000000000000000, 0.000000000000000000 ) ) ;
#12846=CARTESIAN_POINT ( 'NONE',  ( -1.989999999999999991, 9.000000000000000000, -7.500000000000000000 ) ) ;
#12847=DIRECTION ( 'NONE',  ( 0.000000000000000000, 0.000000000000000000, 1.000000000000000000 ) ) ;
#12869=CARTESIAN_POINT ( 'NONE',  ( -0.2740810853920948031, 6.782218762059497585, -1.732684817544354550 ) ) ;
#13089=ADVANCED_FACE ( 'NONE', ( #8105 ), #4464, .F. ) ;
#13094=ORIENTED_EDGE ( 'NONE', *, *, #23928, .T. ) ;
#13096=VERTEX_POINT ( 'NONE', #21419 ) ;
#13098=DIRECTION ( 'NONE',  ( 0.000000000000000000, 1.000000000000000000, 0.000000000000000000 ) ) ;
#13116=CARTESIAN_POINT ( 'NONE',  ( -10.35615758860000035, 0.000000000000000000, 7.000000000000000000 ) ) ;
#13149=DIRECTION ( 'NONE',  ( 1.000000000000000000, 0.000000000000000000, 0.000000000000000000 ) ) ;
#13189=DIRECTION ( 'NONE',  ( 0.000000000000000000, 0.000000000000000000, -1.000000000000000000 ) ) ;
#13227=VERTEX_POINT ( 'NONE', #8221 ) ;
#13246=ADVANCED_FACE ( 'NONE', ( #2520 ), #21050, .F. ) ;
#13350=ORIENTED_EDGE ( 'NONE', *, *, #4764, .T. ) ;
#13355=AXIS2_PLACEMENT_3D ( 'NONE', #9840, #22664, #13585 ) ;
#13374=DIRECTION ( 'NONE',  ( 0.000000000000000000, 0.9995485718789889340, 0.03004417505396965102 ) ) ;
#13389=EDGE_CURVE ( 'NONE', #20864, #18414, #15776, .T. ) ;
#13423=CARTESIAN_POINT ( 'NONE',  ( -1.689767423161654181, 6.985088818113795561, 0.4612040785389939224 ) ) ;
#13430=CIRCLE ( 'NONE', #12679, 7.000000000000000000 ) ;
#13433=VERTEX_POINT ( 'NONE', #22075 ) ;
#13508=SPHERICAL_SURFACE ( 'NONE', #5341, 12.50000000000000000 ) ;
#13547=EDGE_CURVE ( 'NONE', #9495, #9372, #23149, .T. ) ;
#13585=DIRECTION ( 'NONE',  ( -0.1989999999999970126, 0.9799994897957861051, 0.000000000000000000 ) ) ;
#13618=VERTEX_POINT ( 'NONE', #19141 ) ;
#13634=ORIENTED_EDGE ( 'NONE', *, *, #22280, .T. ) ;
#13655=DIRECTION ( 'NONE',  ( 1.000000000000000000, 0.000000000000000000, 0.000000000000000000 ) ) ;
#13661=CARTESIAN_POINT ( 'NONE',  ( -1.670944742899670432, 6.980577527795076342, 0.5248963117445855087 ) ) ;
#13745=AXIS2_PLACEMENT_3D ( 'NONE', #12174, #8547, #13981 ) ;
#13778=CARTESIAN_POINT ( 'NONE',  ( -7.500000000000000000, -10.00000000000000000, 0.000000000000000000 ) ) ;
#13781=CARTESIAN_POINT ( 'NONE',  ( 1.215150159706073874, 6.885362815765219580, 1.263354467349552701 ) ) ;
#13849=FACE_OUTER_BOUND ( 'NONE', #17056, .T. ) ;
#13910=CARTESIAN_POINT ( 'NONE',  ( -1.625770310270910901, 6.969985010803154246, 0.6506056477007011729 ) ) ;
#13924=FACE_BOUND ( 'NONE', #23308, .T. ) ;
#13944=ORIENTED_EDGE ( 'NONE', *, *, #22792, .T. ) ;
#13975=DIRECTION ( 'NONE',  ( 1.000000000000000000, 0.000000000000000000, 0.000000000000000000 ) ) ;
#13981=DIRECTION ( 'NONE',  ( 0.000000000000000000, 1.000000000000000000, 0.000000000000000000 ) ) ;
#14002=DIRECTION ( 'NONE',  ( 1.000000000000000000, 0.000000000000000000, 0.000000000000000000 ) ) ;
#14048=FACE_OUTER_BOUND ( 'NONE', #15320, .T. ) ;
#14129=CARTESIAN_POINT ( 'NONE',  ( -1.989999999999999991, 0.000000000000000000, 0.000000000000000000 ) ) ;
#14153=CYLINDRICAL_SURFACE ( 'NONE', #19200, 7.000000000000000000 ) ;
#14316=DIRECTION ( 'NONE',  ( 0.000000000000000000, 1.000000000000000000, 0.000000000000000000 ) ) ;
#14371=ORIENTED_EDGE ( 'NONE', *, *, #22806, .T. ) ;
#14450=ADVANCED_FACE ( 'NONE', ( #8442 ), #6616, .F. ) ;
#14506=CARTESIAN_POINT ( 'NONE',  ( 1.414363803402227227, 6.923393381151994319, 1.035861679437342753 ) ) ;
#14513=UNCERTAINTY_MEASURE_WITH_UNIT (LENGTH_MEASURE( 1.000000000000000082E-05 ), #4478, 'distance_accuracy_value', 'NONE');
#14538=LINE ( 'NONE', #12499, #17125 ) ;
#14605=EDGE_CURVE ( 'NONE', #21993, #22807, #5710, .T. ) ;
#14674=ORIENTED_EDGE ( 'NONE', *, *, #1569, .T. ) ;
#14677=VECTOR ( 'NONE', #7795, 1000.000000000000000 ) ;
#14705=ORIENTED_EDGE ( 'NONE', *, *, #7744, .T. ) ;
#14714=ORIENTED_EDGE ( 'NONE', *, *, #19314, .F. ) ;
#14813=ORIENTED_EDGE ( 'NONE', *, *, #7474, .T. ) ;
#14913=DIRECTION ( 'NONE',  ( 0.000000000000000000, 0.000000000000000000, 1.000000000000000000 ) ) ;
#14969=LINE ( 'NONE', #16676, #17297 ) ;
#15020=ADVANCED_FACE ( 'NONE', ( #2490 ), #13508, .T. ) ;
#15032=ORIENTED_EDGE ( 'NONE', *, *, #10098, .T. ) ;
#15062=CARTESIAN_POINT ( 'NONE',  ( 1.709999999999999964, 9.000000000000000000, -0.3720215047547999476 ) ) ;
#15103=EDGE_CURVE ( 'NONE', #20340, #2076, #15312, .T. ) ;
#15107=ORIENTED_EDGE ( 'NONE', *, *, #23888, .T. ) ;
#15121=ADVANCED_BREP_SHAPE_REPRESENTATION ( '', ( #16648, #4390 ), #17940 ) ;
#15174=ORIENTED_EDGE ( 'NONE', *, *, #18187, .T. ) ;
#15252=ORIENTED_EDGE ( 'NONE', *, *, #1410, .T. ) ;
#15267=CARTESIAN_POINT ( 'NONE',  ( 0.07252675453223388080, 6.777045746367004853, -1.752615158248006511 ) ) ;
#15306=DIRECTION ( 'NONE',  ( 1.000000000000000000, 0.000000000000000000, 0.000000000000000000 ) ) ;
#15312=LINE ( 'NONE', #17026, #4169 ) ;
#15320=EDGE_LOOP ( 'NONE', ( #15615, #19934, #11762, #2774, #14714, #11051 ) ) ;
#15354=CARTESIAN_POINT ( 'NONE',  ( 0.3169597565512499160, 6.785101045795855157, 1.721165433949310763 ) ) ;
#15418=LINE ( 'NONE', #2351, #3363 ) ;
#15428=EDGE_CURVE ( 'NONE', #9475, #2076, #20170, .T. ) ;
#15473=EDGE_CURVE ( 'NONE', #22015, #9475, #16493, .T. ) ;
#15501=DIRECTION ( 'NONE',  ( 0.000000000000000000, 0.000000000000000000, -1.000000000000000000 ) ) ;
#15512=CARTESIAN_POINT ( 'NONE',  ( 0.000000000000000000, -13.00000000000000000, 0.000000000000000000 ) ) ;
#15563=ADVANCED_FACE ( 'NONE', ( #17260 ), #20655, .F. ) ;
#15568=VERTEX_POINT ( 'NONE', #4306 ) ;
#15579=PRODUCT ( 'Rotary Valve Ball', 'Rotary Valve Ball', '', ( #17523 ) ) ;
#15595=CARTESIAN_POINT ( 'NONE',  ( 0.2041544774629323045, 6.780677947102329739, 1.738509534568517090 ) ) ;
#15615=ORIENTED_EDGE ( 'NONE', *, *, #21850, .F. ) ;
#15645=LINE ( 'NONE', #2460, #23434 ) ;
#15706=LINE ( 'NONE', #13778, #20536 ) ;
#15752=CARTESIAN_POINT ( 'NONE',  ( -1.103481847858666542, 6.865278473733852138, -1.376819519320963137 ) ) ;
#15753=FACE_OUTER_BOUND ( 'NONE', #19682, .T. ) ;
#15776=LINE ( 'NONE', #4897, #11949 ) ;
#15790=CARTESIAN_POINT ( 'NONE',  ( 1.709999999999999964, 12.37689379448999993, -0.3720215047547999476 ) ) ;
#15837=CARTESIAN_POINT ( 'NONE',  ( 1.283659224277774236, 6.897942598336115338, 1.193638655190912168 ) ) ;
#15927=DIRECTION ( 'NONE',  ( -1.000000000000000000, 0.000000000000000000, 0.000000000000000000 ) ) ;
#16021=FACE_OUTER_BOUND ( 'NONE', #9593, .T. ) ;
#16082=ORIENTED_EDGE ( 'NONE', *, *, #9972, .F. ) ;
#16100=AXIS2_PLACEMENT_3D ( 'NONE', #8482, #17684, #6409 ) ;
#16143=DIRECTION ( 'NONE',  ( -0.000000000000000000, 1.000000000000000000, 0.000000000000000000 ) ) ;
#16200=AXIS2_PLACEMENT_3D ( 'NONE', #23410, #10355, #17866 ) ;
#16235=CIRCLE ( 'NONE', #2703, 1.750000000000000000 ) ;
#16246=CARTESIAN_POINT ( 'NONE',  ( 1.709999999999999964, 0.000000000000000000, 0.000000000000000000 ) ) ;
#16290=CARTESIAN_POINT ( 'NONE',  ( 0.000000000000000000, -9.000000000000000000, 0.000000000000000000 ) ) ;
#16308=DIRECTION ( 'NONE',  ( 0.000000000000000000, 1.000000000000000000, 0.000000000000000000 ) ) ;
#16456=CARTESIAN_POINT ( 'NONE',  ( 10.35615758860000035, 0.000000000000000000, -7.000000000000000000 ) ) ;
#16493=CIRCLE ( 'NONE', #18826, 12.38248359579000102 ) ;
#16556=CARTESIAN_POINT ( 'NONE',  ( 0.000000000000000000, 9.000000000000000000, 0.000000000000000000 ) ) ;
#16648=MANIFOLD_SOLID_BREP ( 'Stock-MAS-673-1', #20088 ) ;
#16676=CARTESIAN_POINT ( 'NONE',  ( -1.989999999999999991, 9.799994897958001161, 7.500000000000000000 ) ) ;
#16691=APPLICATION_CONTEXT ( 'automotive_design' ) ;
#16731=CARTESIAN_POINT ( 'NONE',  ( 0.7519233154364799443, 6.819034920433882263, -1.581610603952285254 ) ) ;
#16824=LINE ( 'NONE', #12846, #12111 ) ;
#16838=CIRCLE ( 'NONE', #13355, 10.00000000000000000 ) ;
#16923=PRODUCT_DEFINITION_SHAPE ( 'NONE', 'NONE',  #8728 ) ;
#16948=VECTOR ( 'NONE', #23336, 1000.000000000000000 ) ;
#16968=AXIS2_PLACEMENT_3D ( 'NONE', #20843, #2072, #11287 ) ;
#17026=CARTESIAN_POINT ( 'NONE',  ( -1.989999999999999991, 9.000000000000000000, 7.500000000000000000 ) ) ;
#17056=EDGE_LOOP ( 'NONE', ( #13350, #22457, #14813, #13944, #17154, #22850, #14705, #11681, #4292, #12577, #3412, #18449, #1604 ) ) ;
#17100=CARTESIAN_POINT ( 'NONE',  ( 1.738791845199069819, 6.997157444011510741, -0.2287927106351075324 ) ) ;
#17102=ORIENTED_EDGE ( 'NONE', *, *, #11324, .T. ) ;
#17125=VECTOR ( 'NONE', #14316, 1000.000000000000000 ) ;
#17154=ORIENTED_EDGE ( 'NONE', *, *, #13547, .T. ) ;
#17175=ORIENTED_EDGE ( 'NONE', *, *, #15473, .F. ) ;
#17179=CARTESIAN_POINT ( 'NONE',  ( -0.8309130272245487392, 6.827288109812859496, 1.546313273631122476 ) ) ;
#17260=FACE_OUTER_BOUND ( 'NONE', #22079, .T. ) ;
#17285=DIRECTION ( 'NONE',  ( 1.000000000000000000, 0.000000000000000000, 0.000000000000000000 ) ) ;
#17297=VECTOR ( 'NONE', #22366, 1000.000000000000000 ) ;
#17303=CARTESIAN_POINT ( 'NONE',  ( 0.06268874648260357174, 6.777703239720367812, 1.750068228840472750 ) ) ;
#17432=CARTESIAN_POINT ( 'NONE',  ( -0.2217825122820056838, 6.780516198057334520, 1.739291495566667844 ) ) ;
#17460=CARTESIAN_POINT ( 'NONE',  ( 1.709999999999999964, 13.00000000000000000, 7.500000000000000000 ) ) ;
#17487=AXIS2_PLACEMENT_3D ( 'NONE', #22056, #5465, #12847 ) ;
#17521=DIRECTION ( 'NONE',  ( 0.000000000000000000, 0.000000000000000000, 1.000000000000000000 ) ) ;
#17523=PRODUCT_CONTEXT ( 'NONE', #6482, 'mechanical' ) ;
#17549=CARTESIAN_POINT ( 'NONE',  ( -1.183772340028661274, 6.880224493752307602, 1.289604923395413438 ) ) ;
#17585=FACE_OUTER_BOUND ( 'NONE', #3873, .T. ) ;
#17591=CARTESIAN_POINT ( 'NONE',  ( -10.35615758860000035, 0.000000000000000000, -7.000000000000000000 ) ) ;
#17638=CIRCLE ( 'NONE', #2944, 7.000000000000000000 ) ;
#17659=DIRECTION ( 'NONE',  ( -1.000000000000000000, 0.000000000000000000, 0.000000000000000000 ) ) ;
#17684=DIRECTION ( 'NONE',  ( -1.000000000000000000, 0.000000000000000000, 0.000000000000000000 ) ) ;
#17709=DIRECTION ( 'NONE',  ( 1.000000000000000000, 0.000000000000000000, 0.000000000000000000 ) ) ;
#17720=DIRECTION ( 'NONE',  ( 1.000000000000000000, 0.000000000000000000, 0.000000000000000000 ) ) ;
#17866=DIRECTION ( 'NONE',  ( 0.1709999999999925469, 0.9852710287022563573, 0.000000000000000000 ) ) ;
#17879=ORIENTED_EDGE ( 'NONE', *, *, #15103, .T. ) ;
#17890=DIRECTION ( 'NONE',  ( -1.000000000000000000, 0.000000000000000000, 0.000000000000000000 ) ) ;
#17894=DIRECTION ( 'NONE',  ( 0.000000000000000000, 0.7941276157285981352, 0.6077510427281981320 ) ) ;
#17940=( GEOMETRIC_REPRESENTATION_CONTEXT ( 3 ) GLOBAL_UNCERTAINTY_ASSIGNED_CONTEXT ( ( #12539 ) ) GLOBAL_UNIT_ASSIGNED_CONTEXT ( ( #21285, #19712, #8199 ) ) REPRESENTATION_CONTEXT ( 'NONE', 'WORKASPACE' ) );
#17949=DIRECTION ( 'NONE',  ( 0.9771428571428639742, 0.000000000000000000, 0.2125837170026919909 ) ) ;
#17960=AXIS2_PLACEMENT_3D ( 'NONE', #17460, #17709, #1106 ) ;
#17968=AXIS2_PLACEMENT_3D ( 'NONE', #16246, #21711, #18075 ) ;
#17985=EDGE_CURVE ( 'NONE', #9372, #22807, #20632, .T. ) ;
#17986=CARTESIAN_POINT ( 'NONE',  ( 0.000000000000000000, 9.000000000000000000, 0.000000000000000000 ) ) ;
#18049=ORIENTED_EDGE ( 'NONE', *, *, #21996, .T. ) ;
#18051=CARTESIAN_POINT ( 'NONE',  ( -10.35615758860000035, -1.075999958835999899E-14, 7.000000000000000000 ) ) ;
#18060=DIRECTION ( 'NONE',  ( 0.000000000000000000, 1.000000000000000000, 0.000000000000000000 ) ) ;
#18075=DIRECTION ( 'NONE',  ( 0.000000000000000000, 0.7956974229606958993, -0.6056943214969968681 ) ) ;
#18112=CIRCLE ( 'NONE', #20042, 12.49999999999999289 ) ;
#18187=EDGE_CURVE ( 'NONE', #9372, #9495, #4835, .T. ) ;
#18237=CARTESIAN_POINT ( 'NONE',  ( -1.989999999999999991, 9.799994897958001161, -7.500000000000000000 ) ) ;
#18342=ORIENTED_EDGE ( 'NONE', *, *, #13389, .T. ) ;
#18414=VERTEX_POINT ( 'NONE', #15790 ) ;
#18449=ORIENTED_EDGE ( 'NONE', *, *, #763, .T. ) ;
#18518=MECHANICAL_DESIGN_GEOMETRIC_PRESENTATION_REPRESENTATION('',(#23553),#20456);
#18564=CARTESIAN_POINT ( 'NONE',  ( -1.989999999999999991, 9.799994897958001161, 7.500000000000000000 ) ) ;
#18572=EDGE_LOOP ( 'NONE', ( #6302, #15252, #16082, #6647, #15032, #14674, #18049, #15174, #12617, #22874, #20733, #380, #2314 ) ) ;
#18765=SURFACE_SIDE_STYLE ('',( #2300 ) ) ;
#18773=PLANE ( 'NONE',  #9881 ) ;
#18826=AXIS2_PLACEMENT_3D ( 'NONE', #5991, #15306, #13374 ) ;
#18829=AXIS2_PLACEMENT_3D ( 'NONE', #16556, #12814, #20554 ) ;
#18886=DIRECTION ( 'NONE',  ( 0.000000000000000000, 0.000000000000000000, 1.000000000000000000 ) ) ;
#18920=CARTESIAN_POINT ( 'NONE',  ( 0.9039000843164147758, 6.837447795336954570, -1.500112088426254209 ) ) ;
#18981=ORIENTED_EDGE ( 'NONE', *, *, #15428, .T. ) ;
#19027=EDGE_CURVE ( 'NONE', #20904, #10478, #3320, .T. ) ;
#19032=CARTESIAN_POINT ( 'NONE',  ( -1.708192668324312713, 6.989350524238209239, -0.4397697262170950916 ) ) ;
#19073=B_SPLINE_CURVE_WITH_KNOTS ( 'NONE', 3,
 ( #11304, #4143, #17100, #7781, #257, #1974, #20736, #9358, #11540, #18920, #22191, #16731, #2327, #7662, #497, #7899, #15267, #22659, #12869, #3673, #23020, #22899, #6563, #11659, #6068, #6196, #15752, #4635, #23140, #19032, #6436, #19280 ),
 .UNSPECIFIED., .F., .F.,
 ( 4, 2, 2, 2, 2, 2, 2, 2, 2, 2, 2, 2, 2, 2, 2, 4 ),
 ( 0.000000000000000000, 0.06249999999999993061, 0.1249999999999998612, 0.2499999999999998335, 0.3124999999999998890, 0.3437499999999998890, 0.3749999999999998890, 0.4374999999999998335, 0.4999999999999997780, 0.5624999999999996669, 0.5937499999999996669, 0.6093749999999996669, 0.6249999999999996669, 0.7499999999999997780, 0.8749999999999998890, 1.000000000000000000 ),
 .UNSPECIFIED. ) ;
#19075=PRODUCT_DEFINITION_FORMATION_WITH_SPECIFIED_SOURCE ( 'ANY', '', #15579, .NOT_KNOWN. ) ;
#19141=CARTESIAN_POINT ( 'NONE',  ( -1.989999999999999991, 9.000000000000000000, -7.500000000000000000 ) ) ;
#19145=ADVANCED_FACE ( 'NONE', ( #1580 ), #1086, .F. ) ;
#19148=EDGE_LOOP ( 'NONE', ( #15107, #13094, #20152, #23916, #13634, #19714 ) ) ;
#19182=LINE ( 'NONE', #15062, #9425 ) ;
#19200=AXIS2_PLACEMENT_3D ( 'NONE', #3020, #6759, #8836 ) ;
#19215=DIRECTION ( 'NONE',  ( 0.000000000000000000, 1.000000000000000000, 0.000000000000000000 ) ) ;
#19236=ADVANCED_FACE ( 'NONE', ( #13924, #14048 ), #5098, .F. ) ;
#19241=CARTESIAN_POINT ( 'NONE',  ( -1.600067560738497097, 6.964050391730369327, 0.7113046981209643072 ) ) ;
#19280=CARTESIAN_POINT ( 'NONE',  ( -1.750000000000000000, 7.000000000000000000, 0.000000000000000000 ) ) ;
#19281=DIRECTION ( 'NONE',  ( 0.000000000000000000, 1.000000000000000000, 0.000000000000000000 ) ) ;
#19314=EDGE_CURVE ( 'NONE', #7294, #20019, #7019, .T. ) ;
#19371=CARTESIAN_POINT ( 'NONE',  ( -0.6522852588204888225, 6.808683197727685155, 1.625598361106043166 ) ) ;
#19388=DIRECTION ( 'NONE',  ( 0.000000000000000000, 0.000000000000000000, -1.000000000000000000 ) ) ;
#19396=DIRECTION ( 'NONE',  ( 1.000000000000000000, 0.000000000000000000, 0.000000000000000000 ) ) ;
#19478=CARTESIAN_POINT ( 'NONE',  ( -1.989999999999999991, 0.000000000000000000, 0.000000000000000000 ) ) ;
#19479=VERTEX_POINT ( 'NONE', #206 ) ;
#19494=CARTESIAN_POINT ( 'NONE',  ( -0.5912276634582656065, 6.803124766514241806, 1.648605811313639702 ) ) ;
#19682=EDGE_LOOP ( 'NONE', ( #2977, #20789, #7232, #22736 ) ) ;
#19712=( NAMED_UNIT ( * ) PLANE_ANGLE_UNIT ( ) SI_UNIT ( $, .RADIAN. ) );
#19714=ORIENTED_EDGE ( 'NONE', *, *, #19027, .T. ) ;
#19715=DIRECTION ( 'NONE',  ( 0.000000000000000000, 0.000000000000000000, 1.000000000000000000 ) ) ;
#19739=ADVANCED_FACE ( 'NONE', ( #241 ), #18773, .F. ) ;
#19741=CARTESIAN_POINT ( 'NONE',  ( 1.750000000000001110, 7.000000000000000000, 0.1998543250812850336 ) ) ;
#19827=SHAPE_DEFINITION_REPRESENTATION ( #16923, #20207 ) ;
#19841=CARTESIAN_POINT ( 'NONE',  ( 1.750000000000000000, 7.000000000000000000, 0.000000000000000000 ) ) ;
#19875=CIRCLE ( 'NONE', #4783, 1.750000000000000444 ) ;
#19909=CARTESIAN_POINT ( 'NONE',  ( 10.35615758860000035, 0.000000000000000000, 0.000000000000000000 ) ) ;
#19934=ORIENTED_EDGE ( 'NONE', *, *, #2121, .T. ) ;
#20019=VERTEX_POINT ( 'NONE', #21446 ) ;
#20030=AXIS2_PLACEMENT_3D ( 'NONE', #14129, #15927, #17894 ) ;
#20042=AXIS2_PLACEMENT_3D ( 'NONE', #20389, #32, #3674 ) ;
#20088=CLOSED_SHELL ( 'NONE', ( #11362, #1200, #13246, #19739, #13089, #14450, #7152, #2820, #5113, #15563, #21249, #19236, #15020, #19145, #22411 ) ) ;
#20094=CARTESIAN_POINT ( 'NONE',  ( 1.632208092639368724, 6.971545505544572308, 0.6323144000017536515 ) ) ;
#20101=AXIS2_PLACEMENT_3D ( 'NONE', #19909, #11411, #13098 ) ;
#20135=DIRECTION ( 'NONE',  ( 0.000000000000000000, 1.000000000000000000, 0.000000000000000000 ) ) ;
#20152=ORIENTED_EDGE ( 'NONE', *, *, #11324, .F. ) ;
#20170=LINE ( 'NONE', #10959, #23838 ) ;
#20195=CIRCLE ( 'NONE', #2390, 12.50000000000000178 ) ;
#20207=SHAPE_REPRESENTATION ( 'Rotary Valve Ball', ( #4390 ), #17940 ) ;
#20243=CARTESIAN_POINT ( 'NONE',  ( 10.35615758860000035, 0.000000000000000000, 0.000000000000000000 ) ) ;
#20340=VERTEX_POINT ( 'NONE', #4925 ) ;
#20386=CIRCLE ( 'NONE', #20756, 7.000000000000000000 ) ;
#20389=CARTESIAN_POINT ( 'NONE',  ( 0.000000000000000000, 0.000000000000000000, 0.000000000000000000 ) ) ;
#20421=CARTESIAN_POINT ( 'NONE',  ( -10.35615758860000035, 7.000000000000000000, 0.000000000000000000 ) ) ;
#20427=DIRECTION ( 'NONE',  ( 1.000000000000000000, 0.000000000000000000, 0.000000000000000000 ) ) ;
#20456=( GEOMETRIC_REPRESENTATION_CONTEXT ( 3 ) GLOBAL_UNCERTAINTY_ASSIGNED_CONTEXT ( ( #14513 ) ) GLOBAL_UNIT_ASSIGNED_CONTEXT ( ( #4478, #9804, #11866 ) ) REPRESENTATION_CONTEXT ( 'NONE', 'WORKASPACE' ) );
#20477=DIRECTION ( 'NONE',  ( 0.000000000000000000, 0.000000000000000000, -1.000000000000000000 ) ) ;
#20490=CIRCLE ( 'NONE', #20101, 7.000000000000000000 ) ;
#20536=VECTOR ( 'NONE', #11504, 1000.000000000000000 ) ;
#20551=VERTEX_POINT ( 'NONE', #22448 ) ;
#20554=DIRECTION ( 'NONE',  ( 0.9771428571428639742, 0.000000000000000000, -0.2125837170026919909 ) ) ;
#20628=EDGE_CURVE ( 'NONE', #7085, #19479, #15645, .T. ) ;
#20632=LINE ( 'NONE', #21080, #14677 ) ;
#20655=CYLINDRICAL_SURFACE ( 'NONE', #1806, 1.750000000000000000 ) ;
#20733=ORIENTED_EDGE ( 'NONE', *, *, #21850, .T. ) ;
#20736=CARTESIAN_POINT ( 'NONE',  ( 1.394254956788696598, 6.917606337227010904, -1.084076266210869610 ) ) ;
#20756=AXIS2_PLACEMENT_3D ( 'NONE', #5115, #8980, #12496 ) ;
#20789=ORIENTED_EDGE ( 'NONE', *, *, #14605, .T. ) ;
#20823=CARTESIAN_POINT ( 'NONE',  ( -1.304206744018095554, 6.901791827019449599, 1.169639274656592898 ) ) ;
#20843=CARTESIAN_POINT ( 'NONE',  ( 0.000000000000000000, -9.000000000000000000, 0.000000000000000000 ) ) ;
#20864=VERTEX_POINT ( 'NONE', #3902 ) ;
#20902=DIRECTION ( 'NONE',  ( 0.000000000000000000, 1.000000000000000000, 0.000000000000000000 ) ) ;
#20904=VERTEX_POINT ( 'NONE', #11294 ) ;
#20943=CARTESIAN_POINT ( 'NONE',  ( -0.4973687615736275824, 6.795906696827745286, 1.678020886483821972 ) ) ;
#21020=DIRECTION ( 'NONE',  ( 1.000000000000000000, 0.000000000000000000, 0.000000000000000000 ) ) ;
#21050=CYLINDRICAL_SURFACE ( 'NONE', #5376, 7.500000000000000000 ) ;
#21054=EDGE_CURVE ( 'NONE', #2076, #10478, #6185, .T. ) ;
#21080=CARTESIAN_POINT ( 'NONE',  ( 7.500000000000000000, -10.00000000000000000, 0.000000000000000000 ) ) ;
#21244=DIRECTION ( 'NONE',  ( 0.000000000000000000, 1.000000000000000000, 0.000000000000000000 ) ) ;
#21249=ADVANCED_FACE ( 'NONE', ( #2775 ), #14153, .F. ) ;
#21285=( LENGTH_UNIT ( ) NAMED_UNIT ( * ) SI_UNIT ( .MILLI., .METRE. ) );
#21307=CARTESIAN_POINT ( 'NONE',  ( -0.4015214144528502782, 6.789688267195424842, 1.702981870680819521 ) ) ;
#21313=ORIENTED_EDGE ( 'NONE', *, *, #11200, .F. ) ;
#21319=CARTESIAN_POINT ( 'NONE',  ( -12.75000000000000000, 0.000000000000000000, 0.000000000000000000 ) ) ;
#21419=CARTESIAN_POINT ( 'NONE',  ( 10.35615758860000035, 7.000000000000000000, 0.000000000000000000 ) ) ;
#21440=ORIENTED_EDGE ( 'NONE', *, *, #7474, .F. ) ;
#21446=CARTESIAN_POINT ( 'NONE',  ( 10.35615758860000035, 0.000000000000000000, 7.000000000000000000 ) ) ;
#21521=SHAPE_REPRESENTATION_RELATIONSHIP ( 'NONE' , 'NONE' ,  #20207, #15121 ) ;
#21605=LINE ( 'NONE', #3201, #7230 ) ;
#21620=FACE_OUTER_BOUND ( 'NONE', #1296, .T. ) ;
#21663=FACE_OUTER_BOUND ( 'NONE', #1536, .T. ) ;
#21695=DIRECTION ( 'NONE',  ( 1.000000000000000000, 0.000000000000000000, 0.000000000000000000 ) ) ;
#21711=DIRECTION ( 'NONE',  ( 1.000000000000000000, 0.000000000000000000, 0.000000000000000000 ) ) ;
#21785=CARTESIAN_POINT ( 'NONE',  ( 1.547047946228873982, 6.951972372782297072, 0.8197927924581556169 ) ) ;
#21842=DIRECTION ( 'NONE',  ( 0.000000000000000000, 1.000000000000000000, 0.000000000000000000 ) ) ;
#21850=EDGE_CURVE ( 'NONE', #1329, #5868, #20386, .T. ) ;
#21858=AXIS2_PLACEMENT_3D ( 'NONE', #5583, #20135, #9691 ) ;
#21993=VERTEX_POINT ( 'NONE', #5685 ) ;
#21996=EDGE_CURVE ( 'NONE', #13227, #9372, #3388, .T. ) ;
#22015=VERTEX_POINT ( 'NONE', #3532 ) ;
#22056=CARTESIAN_POINT ( 'NONE',  ( 10.35615758860000035, 0.000000000000000000, 0.000000000000000000 ) ) ;
#22075=CARTESIAN_POINT ( 'NONE',  ( -10.35615758860000035, -7.000000000000000000, 0.000000000000000000 ) ) ;
#22079=EDGE_LOOP ( 'NONE', ( #12323, #4013, #17102, #11972, #10200, #8562 ) ) ;
#22157=ORIENTED_EDGE ( 'NONE', *, *, #17985, .T. ) ;
#22191=CARTESIAN_POINT ( 'NONE',  ( 0.8542036545951054993, 6.831035656885031671, -1.528947743710137308 ) ) ;
#22280=EDGE_CURVE ( 'NONE', #959, #20904, #21605, .T. ) ;
#22366=DIRECTION ( 'NONE',  ( 0.000000000000000000, -1.000000000000000000, 0.000000000000000000 ) ) ;
#22411=ADVANCED_FACE ( 'NONE', ( #13849 ), #4534, .T. ) ;
#22448=CARTESIAN_POINT ( 'NONE',  ( -1.989999999999999991, 12.34057940292999866, 0.000000000000000000 ) ) ;
#22457=ORIENTED_EDGE ( 'NONE', *, *, #4509, .T. ) ;
#22471=DIRECTION ( 'NONE',  ( -0.000000000000000000, 1.000000000000000000, 0.000000000000000000 ) ) ;
#22473=CARTESIAN_POINT ( 'NONE',  ( 0.000000000000000000, 0.000000000000000000, 0.000000000000000000 ) ) ;
#22516=PRESENTATION_STYLE_ASSIGNMENT (( #3999 ) ) ;
#22591=DIRECTION ( 'NONE',  ( 1.000000000000000000, 0.000000000000000000, 0.000000000000000000 ) ) ;
#22619=ORIENTED_EDGE ( 'NONE', *, *, #1569, .F. ) ;
#22630=FILL_AREA_STYLE_COLOUR ( '', #1505 ) ;
#22659=CARTESIAN_POINT ( 'NONE',  ( -0.1599369480228318985, 6.778540605024387489, -1.746824606910323707 ) ) ;
#22664=DIRECTION ( 'NONE',  ( 0.000000000000000000, 0.000000000000000000, -1.000000000000000000 ) ) ;
#22736=ORIENTED_EDGE ( 'NONE', *, *, #13547, .F. ) ;
#22792=EDGE_CURVE ( 'NONE', #13433, #9495, #2811, .T. ) ;
#22806=EDGE_CURVE ( 'NONE', #15568, #959, #19073, .T. ) ;
#22807=VERTEX_POINT ( 'NONE', #8386 ) ;
#22811=CARTESIAN_POINT ( 'NONE',  ( 1.709999999999999964, 9.852710287022999225, -7.500000000000000000 ) ) ;
#22850=ORIENTED_EDGE ( 'NONE', *, *, #21996, .F. ) ;
#22874=ORIENTED_EDGE ( 'NONE', *, *, #11622, .T. ) ;
#22899=CARTESIAN_POINT ( 'NONE',  ( -0.5801485360015447013, 6.802422194044264181, -1.651406016847994263 ) ) ;
#22952=CARTESIAN_POINT ( 'NONE',  ( -1.989999999999999991, 13.00000000000000000, 7.500000000000000000 ) ) ;
#22982=CARTESIAN_POINT ( 'NONE',  ( -1.105760685111225161, 6.867277184477957874, 1.356840241705358663 ) ) ;
#23017=ORIENTED_EDGE ( 'NONE', *, *, #11622, .F. ) ;
#23020=CARTESIAN_POINT ( 'NONE',  ( -0.4976720038370057164, 6.795687889532847414, -1.678983103574156699 ) ) ;
#23086=ORIENTED_EDGE ( 'NONE', *, *, #15428, .F. ) ;
#23096=CARTESIAN_POINT ( 'NONE',  ( 0.000000000000000000, 0.000000000000000000, 0.000000000000000000 ) ) ;
#23114=DIRECTION ( 'NONE',  ( 0.000000000000000000, 0.000000000000000000, -1.000000000000000000 ) ) ;
#23140=CARTESIAN_POINT ( 'NONE',  ( -1.540963341621564675, 6.950233192468949106, -0.8594630492748885908 ) ) ;
#23149=CIRCLE ( 'NONE', #4596, 7.500000000000000000 ) ;
#23166=AXIS2_PLACEMENT_3D ( 'NONE', #3254, #22471, #20427 ) ;
#23171=DIRECTION ( 'NONE',  ( 0.000000000000000000, 0.000000000000000000, -1.000000000000000000 ) ) ;
#23275=EDGE_CURVE ( 'NONE', #13618, #20340, #16824, .T. ) ;
#23308=EDGE_LOOP ( 'NONE', ( #4727, #14371 ) ) ;
#23330=CARTESIAN_POINT ( 'NONE',  ( -10.35615758860000035, 0.000000000000000000, -7.000000000000000000 ) ) ;
#23336=DIRECTION ( 'NONE',  ( 0.000000000000000000, -1.000000000000000000, 0.000000000000000000 ) ) ;
#23410=CARTESIAN_POINT ( 'NONE',  ( 0.000000000000000000, 0.000000000000000000, 7.500000000000000000 ) ) ;
#23423=ORIENTED_EDGE ( 'NONE', *, *, #511, .F. ) ;
#23434=VECTOR ( 'NONE', #9735, 1000.000000000000000 ) ;
#23488=DIRECTION ( 'NONE',  ( 0.000000000000000000, 0.000000000000000000, 1.000000000000000000 ) ) ;
#23553=STYLED_ITEM ( 'NONE', ( #22516 ), #16648 ) ;
#23689=DIRECTION ( 'NONE',  ( -0.1592000000000055038, 0.9872463522343337683, 0.000000000000000000 ) ) ;
#23825=VECTOR ( 'NONE', #15501, 1000.000000000000000 ) ;
#23838=VECTOR ( 'NONE', #10731, 1000.000000000000000 ) ;
#23856=DIRECTION ( 'NONE',  ( 0.000000000000000000, 0.000000000000000000, 1.000000000000000000 ) ) ;
#23888=EDGE_CURVE ( 'NONE', #10478, #22015, #14538, .T. ) ;
#23908=ORIENTED_EDGE ( 'NONE', *, *, #4350, .T. ) ;
#23916=ORIENTED_EDGE ( 'NONE', *, *, #3293, .F. ) ;
#23928=EDGE_CURVE ( 'NONE', #22015, #2993, #19875, .T. ) ;
ENDSEC;
END-ISO-10303-21;
